ISO-10303-21;
HEADER;
FILE_DESCRIPTION (('STEP AP214'),
    '1' );
FILE_NAME ('14. Sleeve.step',
    '2026-10-09T14:04:53',
    ( '' ),
    ( '' ),
    'SwSTEP 2.0',
    'SolidWorks 2021',
    '' );
FILE_SCHEMA (( 'AUTOMOTIVE_DESIGN' ));
ENDSEC;

DATA;
#142=SURFACE_SIDE_STYLE ('',( #56810 ) ) ;
#148=( LENGTH_UNIT ( ) NAMED_UNIT ( * ) SI_UNIT ( .MILLI., .METRE. ) );
#215=ORIENTED_EDGE ( 'NONE', *, *, #91369, .F. ) ;
#282=AXIS2_PLACEMENT_3D ( 'NONE', #75371, #11159, #84548 ) ;
#400=CARTESIAN_POINT ( 'NONE',  ( 28.99999999999999645, 6.123233995736765296E-16, -4.999999999999999112 ) ) ;
#584=CYLINDRICAL_SURFACE ( 'NONE', #102404, 9.000000000000000000 ) ;
#668=SURFACE_STYLE_USAGE ( .BOTH. , #81606 ) ;
#816=SURFACE_STYLE_USAGE ( .BOTH. , #48859 ) ;
#1139=EDGE_LOOP ( 'NONE', ( #15242, #12006 ) ) ;
#1197=CARTESIAN_POINT ( 'NONE',  ( 30.00000000000000000, 0.000000000000000000, 0.000000000000000000 ) ) ;
#1794=CARTESIAN_POINT ( 'NONE',  ( -28.99999999999998934, 1.102182119232617714E-15, 9.000000000000000000 ) ) ;
#2238=LINE ( 'NONE', #84243, #5874 ) ;
#2976=CARTESIAN_POINT ( 'NONE',  ( -30.00000000000000000, 0.000000000000000000, 5.999999999999998224 ) ) ;
#3052=DIRECTION ( 'NONE',  ( 1.000000000000000000, 0.000000000000000000, 0.000000000000000000 ) ) ;
#3067=( LENGTH_UNIT ( ) NAMED_UNIT ( * ) SI_UNIT ( .MILLI., .METRE. ) );
#3089=FILL_AREA_STYLE_COLOUR ( '', #103653 ) ;
#3367=SURFACE_STYLE_USAGE ( .BOTH. , #69178 ) ;
#3612=CYLINDRICAL_SURFACE ( 'NONE', #80511, 9.000000000000000000 ) ;
#3633=FILL_AREA_STYLE ('',( #20401 ) ) ;
#3786=DIRECTION ( 'NONE',  ( 1.000000000000000000, 0.000000000000000000, 0.000000000000000000 ) ) ;
#3894=ORIENTED_EDGE ( 'NONE', *, *, #39756, .T. ) ;
#4137=EDGE_CURVE ( 'NONE', #51789, #56343, #47409, .T. ) ;
#4449=ADVANCED_FACE ( 'NONE', ( #22527 ), #47645, .T. ) ;
#4599=APPLICATION_CONTEXT ( 'automotive_design' ) ;
#4978=MECHANICAL_DESIGN_GEOMETRIC_PRESENTATION_REPRESENTATION('',(#34266),#82506);
#5132=VECTOR ( 'NONE', #77409, 1000.000000000000000 ) ;
#5261=CIRCLE ( 'NONE', #41367, 9.000000000000000000 ) ;
#5423=COLOUR_RGB ( '', 0.09019608, 0.27058824, 0.51372549) ;
#5582=SURFACE_STYLE_FILL_AREA ( #22335 ) ;
#5595=CARTESIAN_POINT ( 'NONE',  ( -29.00000000000000355, 0.000000000000000000, 0.000000000000000000 ) ) ;
#5874=VECTOR ( 'NONE', #51324, 1000.000000000000000 ) ;
#6178=CIRCLE ( 'NONE', #18228, 4.999999999999999112 ) ;
#6179=DIRECTION ( 'NONE',  ( 0.000000000000000000, 0.000000000000000000, -1.000000000000000000 ) ) ;
#6413=CARTESIAN_POINT ( 'NONE',  ( 30.00000000000000000, 9.797174393178835518E-16, -8.000000000000007105 ) ) ;
#6518=STYLED_ITEM ( 'NONE', ( #70521 ), #4449 ) ;
#6784=CONICAL_SURFACE ( 'NONE', #65391, 4.999999999999999112, 0.7853981633974543852 ) ;
#6904=AXIS2_PLACEMENT_3D ( 'NONE', #89182, #19050, #84806 ) ;
#7412=CARTESIAN_POINT ( 'NONE',  ( 29.00000000000001066, 0.000000000000000000, 0.000000000000000000 ) ) ;
#7458=ORIENTED_EDGE ( 'NONE', *, *, #66023, .T. ) ;
#7482=( GEOMETRIC_REPRESENTATION_CONTEXT ( 3 ) GLOBAL_UNCERTAINTY_ASSIGNED_CONTEXT ( ( #101204 ) ) GLOBAL_UNIT_ASSIGNED_CONTEXT ( ( #14337, #57448, #90367 ) ) REPRESENTATION_CONTEXT ( 'NONE', 'WORKASPACE' ) );
#7727=FILL_AREA_STYLE ('',( #58420 ) ) ;
#8379=FILL_AREA_STYLE_COLOUR ( '', #98946 ) ;
#8415=( LENGTH_UNIT ( ) NAMED_UNIT ( * ) SI_UNIT ( .MILLI., .METRE. ) );
#8432=( NAMED_UNIT ( * ) PLANE_ANGLE_UNIT ( ) SI_UNIT ( $, .RADIAN. ) );
#8603=SURFACE_STYLE_FILL_AREA ( #32384 ) ;
#8913=VERTEX_POINT ( 'NONE', #56457 ) ;
#8945=SURFACE_STYLE_FILL_AREA ( #81229 ) ;
#9409=EDGE_LOOP ( 'NONE', ( #55011, #34874, #87903, #31229 ) ) ;
#9517=ORIENTED_EDGE ( 'NONE', *, *, #37779, .F. ) ;
#9836=ORIENTED_EDGE ( 'NONE', *, *, #44877, .F. ) ;
#9847=DIRECTION ( 'NONE',  ( -1.000000000000000000, -0.000000000000000000, -0.000000000000000000 ) ) ;
#9949=DIRECTION ( 'NONE',  ( 0.000000000000000000, 0.000000000000000000, -1.000000000000000000 ) ) ;
#10078=ORIENTED_EDGE ( 'NONE', *, *, #89855, .F. ) ;
#10182=AXIS2_PLACEMENT_3D ( 'NONE', #28573, #21033, #86799 ) ;
#10262=DIRECTION ( 'NONE',  ( 0.000000000000000000, 0.000000000000000000, -1.000000000000000000 ) ) ;
#10635=( NAMED_UNIT ( * ) SI_UNIT ( $, .STERADIAN. ) SOLID_ANGLE_UNIT ( ) );
#10728=AXIS2_PLACEMENT_3D ( 'NONE', #14983, #57033, #47878 ) ;
#10881=( NAMED_UNIT ( * ) SI_UNIT ( $, .STERADIAN. ) SOLID_ANGLE_UNIT ( ) );
#11144=MECHANICAL_DESIGN_GEOMETRIC_PRESENTATION_REPRESENTATION('',(#88623),#57639);
#11159=DIRECTION ( 'NONE',  ( 1.000000000000000000, -0.000000000000000000, -0.000000000000000000 ) ) ;
#11534=CARTESIAN_POINT ( 'NONE',  ( -30.00000000000000000, 0.000000000000000000, 0.000000000000000000 ) ) ;
#11674=DIRECTION ( 'NONE',  ( -1.000000000000000000, -0.000000000000000000, -0.000000000000000000 ) ) ;
#11697=SURFACE_STYLE_USAGE ( .BOTH. , #45165 ) ;
#12006=ORIENTED_EDGE ( 'NONE', *, *, #77250, .T. ) ;
#12032=AXIS2_PLACEMENT_3D ( 'NONE', #5595, #39039, #38518 ) ;
#12298=ORIENTED_EDGE ( 'NONE', *, *, #18103, .F. ) ;
#12549=( NAMED_UNIT ( * ) SI_UNIT ( $, .STERADIAN. ) SOLID_ANGLE_UNIT ( ) );
#12554=CARTESIAN_POINT ( 'NONE',  ( 30.00000000000000000, 0.000000000000000000, 0.000000000000000000 ) ) ;
#12683=VECTOR ( 'NONE', #34215, 1000.000000000000000 ) ;
#12692=UNCERTAINTY_MEASURE_WITH_UNIT (LENGTH_MEASURE( 1.000000000000000082E-05 ), #65789, 'distance_accuracy_value', 'NONE');
#12791=CARTESIAN_POINT ( 'NONE',  ( -28.99999999999998934, 0.000000000000000000, 0.000000000000000000 ) ) ;
#12829=DIRECTION ( 'NONE',  ( 0.7071067811865431318, 8.659560562354987092E-17, 0.7071067811865517916 ) ) ;
#13100=LINE ( 'NONE', #31459, #57286 ) ;
#13254=( NAMED_UNIT ( * ) SI_UNIT ( $, .STERADIAN. ) SOLID_ANGLE_UNIT ( ) );
#13595=VECTOR ( 'NONE', #61871, 1000.000000000000000 ) ;
#13634=CIRCLE ( 'NONE', #99716, 6.000000000000012434 ) ;
#13667=DIRECTION ( 'NONE',  ( 0.000000000000000000, 0.000000000000000000, 1.000000000000000000 ) ) ;
#14054=PRODUCT ( '14. Sleeve', '14. Sleeve', '', ( #41163 ) ) ;
#14189=( NAMED_UNIT ( * ) PLANE_ANGLE_UNIT ( ) SI_UNIT ( $, .RADIAN. ) );
#14337=( LENGTH_UNIT ( ) NAMED_UNIT ( * ) SI_UNIT ( .MILLI., .METRE. ) );
#14373=AXIS2_PLACEMENT_3D ( 'NONE', #69185, #9847, #51373 ) ;
#14472=CARTESIAN_POINT ( 'NONE',  ( 28.99999999999999645, 0.000000000000000000, 0.000000000000000000 ) ) ;
#14556=DIRECTION ( 'NONE',  ( -1.000000000000000000, -0.000000000000000000, -0.000000000000000000 ) ) ;
#14741=SHAPE_DEFINITION_REPRESENTATION ( #61402, #81203 ) ;
#14917=AXIS2_PLACEMENT_3D ( 'NONE', #12791, #38691, #21457 ) ;
#14983=CARTESIAN_POINT ( 'NONE',  ( 0.000000000000000000, 0.000000000000000000, 0.000000000000000000 ) ) ;
#15102=SURFACE_STYLE_USAGE ( .BOTH. , #96572 ) ;
#15242=ORIENTED_EDGE ( 'NONE', *, *, #44877, .T. ) ;
#15243=ADVANCED_FACE ( 'NONE', ( #94666 ), #44210, .T. ) ;
#15836=( NAMED_UNIT ( * ) PLANE_ANGLE_UNIT ( ) SI_UNIT ( $, .RADIAN. ) );
#15982=( NAMED_UNIT ( * ) SI_UNIT ( $, .STERADIAN. ) SOLID_ANGLE_UNIT ( ) );
#16036=ORIENTED_EDGE ( 'NONE', *, *, #61300, .F. ) ;
#16176=EDGE_CURVE ( 'NONE', #19689, #47334, #2238, .T. ) ;
#16357=SURFACE_STYLE_USAGE ( .BOTH. , #142 ) ;
#17121=AXIS2_PLACEMENT_3D ( 'NONE', #105187, #14556, #55544 ) ;
#17125=FILL_AREA_STYLE ('',( #26317 ) ) ;
#17249=ORIENTED_EDGE ( 'NONE', *, *, #66554, .T. ) ;
#17386=DIRECTION ( 'NONE',  ( 1.000000000000000000, -0.000000000000000000, -0.000000000000000000 ) ) ;
#17664=CARTESIAN_POINT ( 'NONE',  ( -29.00000000000000355, 0.000000000000000000, 0.000000000000000000 ) ) ;
#17898=FILL_AREA_STYLE ('',( #84740 ) ) ;
#17926=EDGE_LOOP ( 'NONE', ( #26235, #32675, #23606, #75783 ) ) ;
#18041=EDGE_LOOP ( 'NONE', ( #56712, #57927 ) ) ;
#18103=EDGE_CURVE ( 'NONE', #58408, #51789, #19716, .T. ) ;
#18161=UNCERTAINTY_MEASURE_WITH_UNIT (LENGTH_MEASURE( 1.000000000000000082E-05 ), #48351, 'distance_accuracy_value', 'NONE');
#18228=AXIS2_PLACEMENT_3D ( 'NONE', #14472, #63603, #55465 ) ;
#18435=SURFACE_STYLE_USAGE ( .BOTH. , #75030 ) ;
#18657=ADVANCED_FACE ( 'NONE', ( #48299 ), #36815, .F. ) ;
#18782=PRESENTATION_STYLE_ASSIGNMENT (( #43020 ) ) ;
#18786=DIRECTION ( 'NONE',  ( 0.000000000000000000, 0.000000000000000000, 1.000000000000000000 ) ) ;
#19011=LINE ( 'NONE', #101482, #25028 ) ;
#19043=SURFACE_SIDE_STYLE ('',( #50810 ) ) ;
#19050=DIRECTION ( 'NONE',  ( 1.000000000000000000, 0.000000000000000000, 0.000000000000000000 ) ) ;
#19206=( GEOMETRIC_REPRESENTATION_CONTEXT ( 3 ) GLOBAL_UNCERTAINTY_ASSIGNED_CONTEXT ( ( #90381 ) ) GLOBAL_UNIT_ASSIGNED_CONTEXT ( ( #69919, #102279, #13254 ) ) REPRESENTATION_CONTEXT ( 'NONE', 'WORKASPACE' ) );
#19335=MANIFOLD_SOLID_BREP ( 'Chamfer1', #56606 ) ;
#19689=VERTEX_POINT ( 'NONE', #41864 ) ;
#19695=( GEOMETRIC_REPRESENTATION_CONTEXT ( 3 ) GLOBAL_UNCERTAINTY_ASSIGNED_CONTEXT ( ( #29806 ) ) GLOBAL_UNIT_ASSIGNED_CONTEXT ( ( #47658, #100995, #85351 ) ) REPRESENTATION_CONTEXT ( 'NONE', 'WORKASPACE' ) );
#19716=CIRCLE ( 'NONE', #105806, 8.000000000000007105 ) ;
#19835=SURFACE_STYLE_USAGE ( .BOTH. , #85602 ) ;
#19896=SURFACE_STYLE_FILL_AREA ( #87251 ) ;
#20125=SURFACE_STYLE_FILL_AREA ( #101529 ) ;
#20181=FILL_AREA_STYLE ('',( #85953 ) ) ;
#20401=FILL_AREA_STYLE_COLOUR ( '', #89557 ) ;
#20913=EDGE_CURVE ( 'NONE', #85839, #8913, #13100, .T. ) ;
#20950=( GEOMETRIC_REPRESENTATION_CONTEXT ( 3 ) GLOBAL_UNCERTAINTY_ASSIGNED_CONTEXT ( ( #40829 ) ) GLOBAL_UNIT_ASSIGNED_CONTEXT ( ( #61928, #36076, #68949 ) ) REPRESENTATION_CONTEXT ( 'NONE', 'WORKASPACE' ) );
#20959=SURFACE_STYLE_USAGE ( .BOTH. , #69985 ) ;
#21033=DIRECTION ( 'NONE',  ( 1.000000000000000000, 0.000000000000000000, 0.000000000000000000 ) ) ;
#21457=DIRECTION ( 'NONE',  ( 0.000000000000000000, 0.000000000000000000, -1.000000000000000000 ) ) ;
#21468=SURFACE_SIDE_STYLE ('',( #19896 ) ) ;
#21485=ORIENTED_EDGE ( 'NONE', *, *, #84552, .T. ) ;
#21517=COLOUR_RGB ( '', 0.31764706, 0.68627451, 0.89019608) ;
#21934=CARTESIAN_POINT ( 'NONE',  ( 30.00000000000000000, 1.102182119232617714E-15, -9.000000000000000000 ) ) ;
#22025=VERTEX_POINT ( 'NONE', #97450 ) ;
#22280=CARTESIAN_POINT ( 'NONE',  ( 28.99999999999999645, 0.000000000000000000, 0.000000000000000000 ) ) ;
#22335=FILL_AREA_STYLE ('',( #104274 ) ) ;
#22527=FACE_OUTER_BOUND ( 'NONE', #74051, .T. ) ;
#23014=( GEOMETRIC_REPRESENTATION_CONTEXT ( 3 ) GLOBAL_UNCERTAINTY_ASSIGNED_CONTEXT ( ( #47826 ) ) GLOBAL_UNIT_ASSIGNED_CONTEXT ( ( #26078, #59474, #10881 ) ) REPRESENTATION_CONTEXT ( 'NONE', 'WORKASPACE' ) );
#23015=MECHANICAL_DESIGN_GEOMETRIC_PRESENTATION_REPRESENTATION('',(#66232),#7482);
#23606=ORIENTED_EDGE ( 'NONE', *, *, #69941, .T. ) ;
#23654=( GEOMETRIC_REPRESENTATION_CONTEXT ( 3 ) GLOBAL_UNCERTAINTY_ASSIGNED_CONTEXT ( ( #31055 ) ) GLOBAL_UNIT_ASSIGNED_CONTEXT ( ( #3067, #14189, #84529 ) ) REPRESENTATION_CONTEXT ( 'NONE', 'WORKASPACE' ) );
#23909=CIRCLE ( 'NONE', #37701, 5.999999999999998224 ) ;
#24298=( NAMED_UNIT ( * ) PLANE_ANGLE_UNIT ( ) SI_UNIT ( $, .RADIAN. ) );
#24530=EDGE_LOOP ( 'NONE', ( #45944, #67845, #70269, #97050 ) ) ;
#24546=ADVANCED_FACE ( 'NONE', ( #69414 ), #3612, .T. ) ;
#25020=PRESENTATION_STYLE_ASSIGNMENT (( #668 ) ) ;
#25028=VECTOR ( 'NONE', #84765, 1000.000000000000000 ) ;
#25183=SURFACE_STYLE_USAGE ( .BOTH. , #56972 ) ;
#25196=UNCERTAINTY_MEASURE_WITH_UNIT (LENGTH_MEASURE( 1.000000000000000082E-05 ), #83193, 'distance_accuracy_value', 'NONE');
#25703=CONICAL_SURFACE ( 'NONE', #72164, 4.999999999999999112, 0.7853981633974543852 ) ;
#26078=( LENGTH_UNIT ( ) NAMED_UNIT ( * ) SI_UNIT ( .MILLI., .METRE. ) );
#26235=ORIENTED_EDGE ( 'NONE', *, *, #49341, .F. ) ;
#26317=FILL_AREA_STYLE_COLOUR ( '', #65661 ) ;
#26328=ADVANCED_FACE ( 'NONE', ( #49396, #65063 ), #41846, .F. ) ;
#26617=FACE_OUTER_BOUND ( 'NONE', #102214, .T. ) ;
#27376=CIRCLE ( 'NONE', #54861, 4.999999999999999112 ) ;
#27377=DIRECTION ( 'NONE',  ( 1.000000000000000000, -0.000000000000000000, -0.000000000000000000 ) ) ;
#27414=SURFACE_SIDE_STYLE ('',( #93167 ) ) ;
#27568=CARTESIAN_POINT ( 'NONE',  ( 28.99999999999999645, 0.000000000000000000, 0.000000000000000000 ) ) ;
#27981=ADVANCED_FACE ( 'NONE', ( #52360 ), #584, .T. ) ;
#28260=FACE_OUTER_BOUND ( 'NONE', #32200, .T. ) ;
#28427=CARTESIAN_POINT ( 'NONE',  ( 30.00000000000000000, 0.000000000000000000, 0.000000000000000000 ) ) ;
#28573=CARTESIAN_POINT ( 'NONE',  ( -30.00000000000000000, 0.000000000000000000, 0.000000000000000000 ) ) ;
#28621=VERTEX_POINT ( 'NONE', #78478 ) ;
#29058=PRESENTATION_STYLE_ASSIGNMENT (( #77015 ) ) ;
#29103=CARTESIAN_POINT ( 'NONE',  ( -29.00000000000000355, 0.000000000000000000, 4.999999999999999112 ) ) ;
#29280=ORIENTED_EDGE ( 'NONE', *, *, #69941, .F. ) ;
#29519=LINE ( 'NONE', #95284, #13595 ) ;
#29563=( LENGTH_UNIT ( ) NAMED_UNIT ( * ) SI_UNIT ( .MILLI., .METRE. ) );
#29806=UNCERTAINTY_MEASURE_WITH_UNIT (LENGTH_MEASURE( 1.000000000000000082E-05 ), #47658, 'distance_accuracy_value', 'NONE');
#31055=UNCERTAINTY_MEASURE_WITH_UNIT (LENGTH_MEASURE( 1.000000000000000082E-05 ), #3067, 'distance_accuracy_value', 'NONE');
#31112=SURFACE_STYLE_FILL_AREA ( #81716 ) ;
#31166=CARTESIAN_POINT ( 'NONE',  ( 30.00000000000000000, 0.000000000000000000, 8.000000000000007105 ) ) ;
#31229=ORIENTED_EDGE ( 'NONE', *, *, #39756, .F. ) ;
#31459=CARTESIAN_POINT ( 'NONE',  ( 30.00000000000000000, 6.123233995736765296E-16, -4.999999999999999112 ) ) ;
#31494=CARTESIAN_POINT ( 'NONE',  ( 29.00000000000001066, 0.000000000000000000, 0.000000000000000000 ) ) ;
#31515=ADVANCED_FACE ( 'NONE', ( #37798 ), #25703, .F. ) ;
#31662=DIRECTION ( 'NONE',  ( 0.000000000000000000, 0.000000000000000000, -1.000000000000000000 ) ) ;
#31719=ORIENTED_EDGE ( 'NONE', *, *, #16176, .F. ) ;
#31728=EDGE_CURVE ( 'NONE', #22025, #83401, #13634, .T. ) ;
#32010=DIRECTION ( 'NONE',  ( -1.000000000000000000, 0.000000000000000000, 0.000000000000000000 ) ) ;
#32200=EDGE_LOOP ( 'NONE', ( #68730, #47911, #37171, #71567 ) ) ;
#32241=ADVANCED_FACE ( 'NONE', ( #28260 ), #6784, .F. ) ;
#32384=FILL_AREA_STYLE ('',( #64728 ) ) ;
#32585=SURFACE_STYLE_FILL_AREA ( #82155 ) ;
#32675=ORIENTED_EDGE ( 'NONE', *, *, #77849, .F. ) ;
#33115=DIRECTION ( 'NONE',  ( 0.000000000000000000, 0.000000000000000000, 1.000000000000000000 ) ) ;
#33549=DIRECTION ( 'NONE',  ( 0.000000000000000000, 0.000000000000000000, 1.000000000000000000 ) ) ;
#33614=ADVANCED_FACE ( 'NONE', ( #56616 ), #104646, .F. ) ;
#33890=( NAMED_UNIT ( * ) PLANE_ANGLE_UNIT ( ) SI_UNIT ( $, .RADIAN. ) );
#34050=CARTESIAN_POINT ( 'NONE',  ( -30.00000000000000000, 0.000000000000000000, 0.000000000000000000 ) ) ;
#34215=DIRECTION ( 'NONE',  ( 0.7071067811865456854, 8.659560562354955045E-17, 0.7071067811865493491 ) ) ;
#34241=STYLED_ITEM ( 'NONE', ( #39757 ), #31515 ) ;
#34266=STYLED_ITEM ( 'NONE', ( #44357 ), #68817 ) ;
#34271=ADVANCED_FACE ( 'NONE', ( #101269 ), #68870, .F. ) ;
#34311=( GEOMETRIC_REPRESENTATION_CONTEXT ( 3 ) GLOBAL_UNCERTAINTY_ASSIGNED_CONTEXT ( ( #18161 ) ) GLOBAL_UNIT_ASSIGNED_CONTEXT ( ( #48351, #8432, #98497 ) ) REPRESENTATION_CONTEXT ( 'NONE', 'WORKASPACE' ) );
#34343=AXIS2_PLACEMENT_3D ( 'NONE', #1197, #84812, #36311 ) ;
#34531=ADVANCED_BREP_SHAPE_REPRESENTATION ( '', ( #19335, #10728 ), #66095 ) ;
#34874=ORIENTED_EDGE ( 'NONE', *, *, #61300, .T. ) ;
#35671=FILL_AREA_STYLE_COLOUR ( '', #63561 ) ;
#35699=( NAMED_UNIT ( * ) PLANE_ANGLE_UNIT ( ) SI_UNIT ( $, .RADIAN. ) );
#35704=CARTESIAN_POINT ( 'NONE',  ( -30.00000000000000000, 1.040949779275249548E-15, 7.999999999999986677 ) ) ;
#36039=PRESENTATION_STYLE_ASSIGNMENT (( #11697 ) ) ;
#36076=( NAMED_UNIT ( * ) PLANE_ANGLE_UNIT ( ) SI_UNIT ( $, .RADIAN. ) );
#36311=DIRECTION ( 'NONE',  ( 0.000000000000000000, 0.000000000000000000, 1.000000000000000000 ) ) ;
#36466=ORIENTED_EDGE ( 'NONE', *, *, #84552, .F. ) ;
#36549=DIRECTION ( 'NONE',  ( 0.000000000000000000, 0.000000000000000000, -1.000000000000000000 ) ) ;
#36815=CONICAL_SURFACE ( 'NONE', #83268, 5.999999999999998224, 0.7853981633974509435 ) ;
#37171=ORIENTED_EDGE ( 'NONE', *, *, #101768, .T. ) ;
#37701=AXIS2_PLACEMENT_3D ( 'NONE', #34050, #51239, #10262 ) ;
#37779=EDGE_CURVE ( 'NONE', #58408, #19689, #67092, .T. ) ;
#37798=FACE_OUTER_BOUND ( 'NONE', #92361, .T. ) ;
#37922=MECHANICAL_DESIGN_GEOMETRIC_PRESENTATION_REPRESENTATION('',(#48185),#98166);
#38157=CARTESIAN_POINT ( 'NONE',  ( 30.00000000000000000, 0.000000000000000000, 8.000000000000007105 ) ) ;
#38518=DIRECTION ( 'NONE',  ( 0.000000000000000000, 0.000000000000000000, -1.000000000000000000 ) ) ;
#38691=DIRECTION ( 'NONE',  ( 1.000000000000000000, -0.000000000000000000, -0.000000000000000000 ) ) ;
#39039=DIRECTION ( 'NONE',  ( -1.000000000000000000, -0.000000000000000000, -0.000000000000000000 ) ) ;
#39096=ORIENTED_EDGE ( 'NONE', *, *, #46430, .F. ) ;
#39123=ORIENTED_EDGE ( 'NONE', *, *, #20913, .T. ) ;
#39225=( NAMED_UNIT ( * ) PLANE_ANGLE_UNIT ( ) SI_UNIT ( $, .RADIAN. ) );
#39444=ORIENTED_EDGE ( 'NONE', *, *, #66023, .F. ) ;
#39756=EDGE_CURVE ( 'NONE', #88153, #76051, #29519, .T. ) ;
#39757=PRESENTATION_STYLE_ASSIGNMENT (( #25183 ) ) ;
#39802=MECHANICAL_DESIGN_GEOMETRIC_PRESENTATION_REPRESENTATION('',(#89760),#19206);
#39811=DIRECTION ( 'NONE',  ( 0.000000000000000000, 0.000000000000000000, -1.000000000000000000 ) ) ;
#39916=STYLED_ITEM ( 'NONE', ( #18782 ), #74678 ) ;
#40730=COLOUR_RGB ( '', 0.31764706, 0.68627451, 0.89019608) ;
#40829=UNCERTAINTY_MEASURE_WITH_UNIT (LENGTH_MEASURE( 1.000000000000000082E-05 ), #61928, 'distance_accuracy_value', 'NONE');
#41114=DIRECTION ( 'NONE',  ( 0.000000000000000000, 0.000000000000000000, -1.000000000000000000 ) ) ;
#41163=PRODUCT_CONTEXT ( 'NONE', #4599, 'mechanical' ) ;
#41229=LINE ( 'NONE', #59022, #46600 ) ;
#41331=DIRECTION ( 'NONE',  ( 1.000000000000000000, 0.000000000000000000, 0.000000000000000000 ) ) ;
#41367=AXIS2_PLACEMENT_3D ( 'NONE', #66446, #17386, #41114 ) ;
#41623=DIRECTION ( 'NONE',  ( -1.000000000000000000, -0.000000000000000000, -0.000000000000000000 ) ) ;
#41846=PLANE ( 'NONE',  #96077 ) ;
#41864=CARTESIAN_POINT ( 'NONE',  ( 29.00000000000001066, 0.000000000000000000, 9.000000000000000000 ) ) ;
#42202=SHAPE_REPRESENTATION_RELATIONSHIP ( 'NONE' , 'NONE' ,  #81203, #34531 ) ;
#42661=ORIENTED_EDGE ( 'NONE', *, *, #18103, .T. ) ;
#42739=PRESENTATION_STYLE_ASSIGNMENT (( #58392 ) ) ;
#42934=UNCERTAINTY_MEASURE_WITH_UNIT (LENGTH_MEASURE( 1.000000000000000082E-05 ), #59490, 'distance_accuracy_value', 'NONE');
#42995=ORIENTED_EDGE ( 'NONE', *, *, #50182, .T. ) ;
#43020=SURFACE_STYLE_USAGE ( .BOTH. , #27414 ) ;
#43295=MECHANICAL_DESIGN_GEOMETRIC_PRESENTATION_REPRESENTATION('',(#45016),#20950);
#43746=SURFACE_STYLE_FILL_AREA ( #17898 ) ;
#44067=CARTESIAN_POINT ( 'NONE',  ( 30.00000000000000000, 0.000000000000000000, 0.000000000000000000 ) ) ;
#44210=CONICAL_SURFACE ( 'NONE', #101007, 8.000000000000007105, 0.7853981633974509435 ) ;
#44357=PRESENTATION_STYLE_ASSIGNMENT (( #3367 ) ) ;
#44633=( LENGTH_UNIT ( ) NAMED_UNIT ( * ) SI_UNIT ( .MILLI., .METRE. ) );
#44703=CIRCLE ( 'NONE', #10182, 5.999999999999998224 ) ;
#44877=EDGE_CURVE ( 'NONE', #76301, #57315, #23909, .T. ) ;
#45016=STYLED_ITEM ( 'NONE', ( #29058 ), #19335 ) ;
#45130=DIRECTION ( 'NONE',  ( 0.000000000000000000, 0.000000000000000000, -1.000000000000000000 ) ) ;
#45165=SURFACE_SIDE_STYLE ('',( #84551 ) ) ;
#45645=CARTESIAN_POINT ( 'NONE',  ( -28.99999999999998934, 0.000000000000000000, 0.000000000000000000 ) ) ;
#45944=ORIENTED_EDGE ( 'NONE', *, *, #20913, .F. ) ;
#46243=SURFACE_STYLE_FILL_AREA ( #71557 ) ;
#46383=CARTESIAN_POINT ( 'NONE',  ( 28.99999999999999645, 0.000000000000000000, 0.000000000000000000 ) ) ;
#46430=EDGE_CURVE ( 'NONE', #83401, #22025, #105170, .T. ) ;
#46600=VECTOR ( 'NONE', #58488, 1000.000000000000000 ) ;
#47334=VERTEX_POINT ( 'NONE', #64078 ) ;
#47392=CARTESIAN_POINT ( 'NONE',  ( 30.00000000000000000, 1.040949779275250534E-15, -8.000000000000007105 ) ) ;
#47409=LINE ( 'NONE', #6413, #92609 ) ;
#47415=EDGE_LOOP ( 'NONE', ( #42661, #60540 ) ) ;
#47468=EDGE_CURVE ( 'NONE', #28621, #22025, #72141, .T. ) ;
#47645=CONICAL_SURFACE ( 'NONE', #14917, 9.000000000000000000, 0.7853981633974509435 ) ;
#47658=( LENGTH_UNIT ( ) NAMED_UNIT ( * ) SI_UNIT ( .MILLI., .METRE. ) );
#47826=UNCERTAINTY_MEASURE_WITH_UNIT (LENGTH_MEASURE( 1.000000000000000082E-05 ), #26078, 'distance_accuracy_value', 'NONE');
#47869=DIRECTION ( 'NONE',  ( -1.000000000000000000, 0.000000000000000000, 0.000000000000000000 ) ) ;
#47878=DIRECTION ( 'NONE',  ( 1.000000000000000000, 0.000000000000000000, 0.000000000000000000 ) ) ;
#47911=ORIENTED_EDGE ( 'NONE', *, *, #99775, .F. ) ;
#48185=STYLED_ITEM ( 'NONE', ( #36039 ), #34271 ) ;
#48299=FACE_OUTER_BOUND ( 'NONE', #17926, .T. ) ;
#48351=( LENGTH_UNIT ( ) NAMED_UNIT ( * ) SI_UNIT ( .MILLI., .METRE. ) );
#48859=SURFACE_SIDE_STYLE ('',( #8945 ) ) ;
#49341=EDGE_CURVE ( 'NONE', #8913, #57315, #41229, .T. ) ;
#49360=DIRECTION ( 'NONE',  ( -1.000000000000000000, -0.000000000000000000, -0.000000000000000000 ) ) ;
#49378=CIRCLE ( 'NONE', #99343, 7.999999999999986677 ) ;
#49396=FACE_BOUND ( 'NONE', #1139, .T. ) ;
#49733=EDGE_CURVE ( 'NONE', #47334, #76051, #5261, .T. ) ;
#49811=COLOUR_RGB ( '', 0.08235294, 0.09019608, 0.10196078) ;
#50003=SURFACE_STYLE_FILL_AREA ( #17125 ) ;
#50182=EDGE_CURVE ( 'NONE', #76051, #47334, #51825, .T. ) ;
#50239=( LENGTH_UNIT ( ) NAMED_UNIT ( * ) SI_UNIT ( .MILLI., .METRE. ) );
#50518=PLANE ( 'NONE',  #79433 ) ;
#50704=APPLICATION_CONTEXT ( 'automotive_design' ) ;
#50810=SURFACE_STYLE_FILL_AREA ( #100440 ) ;
#51239=DIRECTION ( 'NONE',  ( 1.000000000000000000, 0.000000000000000000, 0.000000000000000000 ) ) ;
#51324=DIRECTION ( 'NONE',  ( -1.000000000000000000, -0.000000000000000000, -0.000000000000000000 ) ) ;
#51373=DIRECTION ( 'NONE',  ( 0.000000000000000000, 0.000000000000000000, 1.000000000000000000 ) ) ;
#51509=EDGE_CURVE ( 'NONE', #19689, #56343, #74442, .T. ) ;
#51527=LINE ( 'NONE', #2976, #5132 ) ;
#51589=STYLED_ITEM ( 'NONE', ( #97602 ), #33614 ) ;
#51608=CIRCLE ( 'NONE', #12032, 4.999999999999999112 ) ;
#51789=VERTEX_POINT ( 'NONE', #47392 ) ;
#51825=CIRCLE ( 'NONE', #89725, 9.000000000000000000 ) ;
#51827=CARTESIAN_POINT ( 'NONE',  ( 30.00000000000000000, 0.000000000000000000, 0.000000000000000000 ) ) ;
#52121=DIRECTION ( 'NONE',  ( 0.000000000000000000, 0.000000000000000000, -1.000000000000000000 ) ) ;
#52125=PRESENTATION_STYLE_ASSIGNMENT (( #69397 ) ) ;
#52163=FILL_AREA_STYLE ('',( #3089 ) ) ;
#52360=FACE_OUTER_BOUND ( 'NONE', #82226, .T. ) ;
#53281=FILL_AREA_STYLE_COLOUR ( '', #5423 ) ;
#53910=DIRECTION ( 'NONE',  ( -0.7071067811865456854, 8.659560562354957510E-17, -0.7071067811865493491 ) ) ;
#54861=AXIS2_PLACEMENT_3D ( 'NONE', #17664, #92600, #85054 ) ;
#54999=ADVANCED_FACE ( 'NONE', ( #99380 ), #97803, .F. ) ;
#55011=ORIENTED_EDGE ( 'NONE', *, *, #66554, .F. ) ;
#55046=EDGE_LOOP ( 'NONE', ( #21485, #39123, #94564, #87959 ) ) ;
#55065=AXIS2_PLACEMENT_3D ( 'NONE', #82751, #73579, #59020 ) ;
#55128=DIRECTION ( 'NONE',  ( 1.000000000000000000, 0.000000000000000000, 0.000000000000000000 ) ) ;
#55182=PRESENTATION_STYLE_ASSIGNMENT (( #19835 ) ) ;
#55330=SURFACE_SIDE_STYLE ('',( #31112 ) ) ;
#55465=DIRECTION ( 'NONE',  ( 0.000000000000000000, 0.000000000000000000, -1.000000000000000000 ) ) ;
#55544=DIRECTION ( 'NONE',  ( 0.000000000000000000, 0.000000000000000000, 1.000000000000000000 ) ) ;
#56343=VERTEX_POINT ( 'NONE', #84708 ) ;
#56457=CARTESIAN_POINT ( 'NONE',  ( -29.00000000000000355, 6.123233995736765296E-16, -4.999999999999999112 ) ) ;
#56518=DIRECTION ( 'NONE',  ( 1.000000000000000000, 0.000000000000000000, 0.000000000000000000 ) ) ;
#56606=CLOSED_SHELL ( 'NONE', ( #15243, #31515, #74678, #34271, #54999, #27981, #103525, #26328, #24546, #33614, #18657, #4449, #32241, #68817 ) ) ;
#56616=FACE_OUTER_BOUND ( 'NONE', #24530, .T. ) ;
#56712=ORIENTED_EDGE ( 'NONE', *, *, #46430, .T. ) ;
#56810=SURFACE_STYLE_FILL_AREA ( #7727 ) ;
#56954=( NAMED_UNIT ( * ) PLANE_ANGLE_UNIT ( ) SI_UNIT ( $, .RADIAN. ) );
#56972=SURFACE_SIDE_STYLE ('',( #99021 ) ) ;
#57033=DIRECTION ( 'NONE',  ( 0.000000000000000000, 0.000000000000000000, 1.000000000000000000 ) ) ;
#57147=( NAMED_UNIT ( * ) SI_UNIT ( $, .STERADIAN. ) SOLID_ANGLE_UNIT ( ) );
#57286=VECTOR ( 'NONE', #64854, 1000.000000000000000 ) ;
#57315=VERTEX_POINT ( 'NONE', #71315 ) ;
#57448=( NAMED_UNIT ( * ) PLANE_ANGLE_UNIT ( ) SI_UNIT ( $, .RADIAN. ) );
#57639=( GEOMETRIC_REPRESENTATION_CONTEXT ( 3 ) GLOBAL_UNCERTAINTY_ASSIGNED_CONTEXT ( ( #67759 ) ) GLOBAL_UNIT_ASSIGNED_CONTEXT ( ( #50239, #35699, #75579 ) ) REPRESENTATION_CONTEXT ( 'NONE', 'WORKASPACE' ) );
#57927=ORIENTED_EDGE ( 'NONE', *, *, #31728, .T. ) ;
#58187=MECHANICAL_DESIGN_GEOMETRIC_PRESENTATION_REPRESENTATION('',(#6518),#104694);
#58392=SURFACE_STYLE_USAGE ( .BOTH. , #19043 ) ;
#58408=VERTEX_POINT ( 'NONE', #38157 ) ;
#58420=FILL_AREA_STYLE_COLOUR ( '', #66131 ) ;
#58488=DIRECTION ( 'NONE',  ( -0.7071067811865456854, 8.659560562354953812E-17, -0.7071067811865493491 ) ) ;
#58534=AXIS2_PLACEMENT_3D ( 'NONE', #60817, #93707, #18786 ) ;
#59020=DIRECTION ( 'NONE',  ( 0.000000000000000000, 0.000000000000000000, -1.000000000000000000 ) ) ;
#59022=CARTESIAN_POINT ( 'NONE',  ( -30.00000000000000000, 7.347880794884117764E-16, -5.999999999999998224 ) ) ;
#59189=COLOUR_RGB ( '', 0.09019608, 0.27058824, 0.51372549) ;
#59474=( NAMED_UNIT ( * ) PLANE_ANGLE_UNIT ( ) SI_UNIT ( $, .RADIAN. ) );
#59490=( LENGTH_UNIT ( ) NAMED_UNIT ( * ) SI_UNIT ( .MILLI., .METRE. ) );
#59901=COLOUR_RGB ( '', 0.09019608, 0.27058824, 0.51372549) ;
#60141=ORIENTED_EDGE ( 'NONE', *, *, #72182, .T. ) ;
#60540=ORIENTED_EDGE ( 'NONE', *, *, #91369, .T. ) ;
#60817=CARTESIAN_POINT ( 'NONE',  ( -30.00000000000000000, 0.000000000000000000, 0.000000000000000000 ) ) ;
#61129=SURFACE_STYLE_FILL_AREA ( #20181 ) ;
#61300=EDGE_CURVE ( 'NONE', #62246, #47334, #75695, .T. ) ;
#61402=PRODUCT_DEFINITION_SHAPE ( 'NONE', 'NONE',  #95727 ) ;
#61785=EDGE_LOOP ( 'NONE', ( #60141, #17249 ) ) ;
#61871=DIRECTION ( 'NONE',  ( 0.7071067811865456854, 0.000000000000000000, -0.7071067811865493491 ) ) ;
#61928=( LENGTH_UNIT ( ) NAMED_UNIT ( * ) SI_UNIT ( .MILLI., .METRE. ) );
#62246=VERTEX_POINT ( 'NONE', #35704 ) ;
#62259=ORIENTED_EDGE ( 'NONE', *, *, #90112, .T. ) ;
#62434=( NAMED_UNIT ( * ) SI_UNIT ( $, .STERADIAN. ) SOLID_ANGLE_UNIT ( ) );
#63182=EDGE_CURVE ( 'NONE', #28621, #102936, #19011, .T. ) ;
#63256=SURFACE_SIDE_STYLE ('',( #61129 ) ) ;
#63367=( GEOMETRIC_REPRESENTATION_CONTEXT ( 3 ) GLOBAL_UNCERTAINTY_ASSIGNED_CONTEXT ( ( #96820 ) ) GLOBAL_UNIT_ASSIGNED_CONTEXT ( ( #8415, #56954, #15982 ) ) REPRESENTATION_CONTEXT ( 'NONE', 'WORKASPACE' ) );
#63561=COLOUR_RGB ( '', 0.72549020, 0.75294118, 0.79215686) ;
#63603=DIRECTION ( 'NONE',  ( 1.000000000000000000, 0.000000000000000000, 0.000000000000000000 ) ) ;
#64078=CARTESIAN_POINT ( 'NONE',  ( -28.99999999999998934, 0.000000000000000000, 9.000000000000000000 ) ) ;
#64383=MECHANICAL_DESIGN_GEOMETRIC_PRESENTATION_REPRESENTATION('',(#93712),#19695);
#64546=PRESENTATION_STYLE_ASSIGNMENT (( #816 ) ) ;
#64728=FILL_AREA_STYLE_COLOUR ( '', #49811 ) ;
#64854=DIRECTION ( 'NONE',  ( -1.000000000000000000, -0.000000000000000000, -0.000000000000000000 ) ) ;
#65053=CARTESIAN_POINT ( 'NONE',  ( -30.00000000000000000, 0.000000000000000000, 5.999999999999998224 ) ) ;
#65063=FACE_OUTER_BOUND ( 'NONE', #61785, .T. ) ;
#65346=ORIENTED_EDGE ( 'NONE', *, *, #37779, .T. ) ;
#65391=AXIS2_PLACEMENT_3D ( 'NONE', #22280, #55128, #88057 ) ;
#65659=ORIENTED_EDGE ( 'NONE', *, *, #72182, .F. ) ;
#65661=COLOUR_RGB ( '', 0.72549020, 0.75294118, 0.79215686) ;
#65789=( LENGTH_UNIT ( ) NAMED_UNIT ( * ) SI_UNIT ( .MILLI., .METRE. ) );
#66023=EDGE_CURVE ( 'NONE', #56343, #19689, #66573, .T. ) ;
#66095=( GEOMETRIC_REPRESENTATION_CONTEXT ( 3 ) GLOBAL_UNCERTAINTY_ASSIGNED_CONTEXT ( ( #25196 ) ) GLOBAL_UNIT_ASSIGNED_CONTEXT ( ( #83193, #91307, #99354 ) ) REPRESENTATION_CONTEXT ( 'NONE', 'WORKASPACE' ) );
#66131=COLOUR_RGB ( '', 0.31764706, 0.68627451, 0.89019608) ;
#66232=STYLED_ITEM ( 'NONE', ( #73636 ), #18657 ) ;
#66446=CARTESIAN_POINT ( 'NONE',  ( -28.99999999999998934, 0.000000000000000000, 0.000000000000000000 ) ) ;
#66554=EDGE_CURVE ( 'NONE', #62246, #88153, #49378, .T. ) ;
#66573=CIRCLE ( 'NONE', #94140, 9.000000000000000000 ) ;
#66674=UNCERTAINTY_MEASURE_WITH_UNIT (LENGTH_MEASURE( 1.000000000000000082E-05 ), #91054, 'distance_accuracy_value', 'NONE');
#67083=COLOUR_RGB ( '', 0.72549020, 0.75294118, 0.79215686) ;
#67092=LINE ( 'NONE', #31166, #92457 ) ;
#67534=EDGE_LOOP ( 'NONE', ( #215, #103926, #82184, #9517 ) ) ;
#67559=FILL_AREA_STYLE_COLOUR ( '', #59189 ) ;
#67564=CONICAL_SURFACE ( 'NONE', #282, 9.000000000000000000, 0.7853981633974509435 ) ;
#67759=UNCERTAINTY_MEASURE_WITH_UNIT (LENGTH_MEASURE( 1.000000000000000082E-05 ), #50239, 'distance_accuracy_value', 'NONE');
#67825=FACE_OUTER_BOUND ( 'NONE', #9409, .T. ) ;
#67845=ORIENTED_EDGE ( 'NONE', *, *, #99775, .T. ) ;
#67904=ORIENTED_EDGE ( 'NONE', *, *, #90112, .F. ) ;
#68371=( NAMED_UNIT ( * ) PLANE_ANGLE_UNIT ( ) SI_UNIT ( $, .RADIAN. ) );
#68730=ORIENTED_EDGE ( 'NONE', *, *, #47468, .F. ) ;
#68817=ADVANCED_FACE ( 'NONE', ( #26617 ), #106587, .T. ) ;
#68870=CONICAL_SURFACE ( 'NONE', #58534, 5.999999999999998224, 0.7853981633974509435 ) ;
#68886=LINE ( 'NONE', #21934, #87697 ) ;
#68949=( NAMED_UNIT ( * ) SI_UNIT ( $, .STERADIAN. ) SOLID_ANGLE_UNIT ( ) );
#69178=SURFACE_SIDE_STYLE ('',( #20125 ) ) ;
#69185=CARTESIAN_POINT ( 'NONE',  ( 30.00000000000000000, 0.000000000000000000, 0.000000000000000000 ) ) ;
#69276=( GEOMETRIC_REPRESENTATION_CONTEXT ( 3 ) GLOBAL_UNCERTAINTY_ASSIGNED_CONTEXT ( ( #66674 ) ) GLOBAL_UNIT_ASSIGNED_CONTEXT ( ( #91054, #33890, #100711 ) ) REPRESENTATION_CONTEXT ( 'NONE', 'WORKASPACE' ) );
#69397=SURFACE_STYLE_USAGE ( .BOTH. , #82908 ) ;
#69414=FACE_OUTER_BOUND ( 'NONE', #85573, .T. ) ;
#69502=STYLED_ITEM ( 'NONE', ( #42739 ), #34531 ) ;
#69749=SURFACE_STYLE_USAGE ( .BOTH. , #63256 ) ;
#69919=( LENGTH_UNIT ( ) NAMED_UNIT ( * ) SI_UNIT ( .MILLI., .METRE. ) );
#69941=EDGE_CURVE ( 'NONE', #102936, #76301, #51527, .T. ) ;
#69985=SURFACE_SIDE_STYLE ('',( #46243 ) ) ;
#70269=ORIENTED_EDGE ( 'NONE', *, *, #63182, .T. ) ;
#70521=PRESENTATION_STYLE_ASSIGNMENT (( #20959 ) ) ;
#70953=ORIENTED_EDGE ( 'NONE', *, *, #47468, .T. ) ;
#71315=CARTESIAN_POINT ( 'NONE',  ( -30.00000000000000000, 7.347880794884117764E-16, -5.999999999999998224 ) ) ;
#71447=CARTESIAN_POINT ( 'NONE',  ( 30.00000000000000000, 0.000000000000000000, 0.000000000000000000 ) ) ;
#71557=FILL_AREA_STYLE ('',( #95858 ) ) ;
#71567=ORIENTED_EDGE ( 'NONE', *, *, #31728, .F. ) ;
#72061=ORIENTED_EDGE ( 'NONE', *, *, #16176, .T. ) ;
#72141=LINE ( 'NONE', #95364, #79366 ) ;
#72164=AXIS2_PLACEMENT_3D ( 'NONE', #46383, #41331, #81769 ) ;
#72182=EDGE_CURVE ( 'NONE', #88153, #62246, #101598, .T. ) ;
#72620=CARTESIAN_POINT ( 'NONE',  ( -30.00000000000000000, 0.000000000000000000, 0.000000000000000000 ) ) ;
#72854=ORIENTED_EDGE ( 'NONE', *, *, #51509, .T. ) ;
#73435=STYLED_ITEM ( 'NONE', ( #25020 ), #15243 ) ;
#73579=DIRECTION ( 'NONE',  ( -1.000000000000000000, -0.000000000000000000, -0.000000000000000000 ) ) ;
#73636=PRESENTATION_STYLE_ASSIGNMENT (( #97382 ) ) ;
#73770=DIRECTION ( 'NONE',  ( 0.000000000000000000, 0.000000000000000000, -1.000000000000000000 ) ) ;
#74051=EDGE_LOOP ( 'NONE', ( #16036, #65659, #3894, #101344 ) ) ;
#74442=CIRCLE ( 'NONE', #91648, 9.000000000000000000 ) ;
#74678=ADVANCED_FACE ( 'NONE', ( #67825 ), #67564, .T. ) ;
#74761=PRODUCT_DEFINITION_CONTEXT ( 'detailed design', #50704, 'design' ) ;
#75030=SURFACE_SIDE_STYLE ('',( #43746 ) ) ;
#75371=CARTESIAN_POINT ( 'NONE',  ( -28.99999999999998934, 0.000000000000000000, 0.000000000000000000 ) ) ;
#75579=( NAMED_UNIT ( * ) SI_UNIT ( $, .STERADIAN. ) SOLID_ANGLE_UNIT ( ) );
#75647=( NAMED_UNIT ( * ) PLANE_ANGLE_UNIT ( ) SI_UNIT ( $, .RADIAN. ) );
#75695=LINE ( 'NONE', #1794, #12683 ) ;
#75783=ORIENTED_EDGE ( 'NONE', *, *, #77250, .F. ) ;
#76051=VERTEX_POINT ( 'NONE', #80952 ) ;
#76173=( NAMED_UNIT ( * ) SI_UNIT ( $, .STERADIAN. ) SOLID_ANGLE_UNIT ( ) );
#76301=VERTEX_POINT ( 'NONE', #65053 ) ;
#76364=UNCERTAINTY_MEASURE_WITH_UNIT (LENGTH_MEASURE( 1.000000000000000082E-05 ), #44633, 'distance_accuracy_value', 'NONE');
#76445=AXIS2_PLACEMENT_3D ( 'NONE', #27568, #3786, #103533 ) ;
#76636=PRESENTATION_STYLE_ASSIGNMENT (( #18435 ) ) ;
#77015=SURFACE_STYLE_USAGE ( .BOTH. , #21468 ) ;
#77062=STYLED_ITEM ( 'NONE', ( #55182 ), #24546 ) ;
#77250=EDGE_CURVE ( 'NONE', #57315, #76301, #44703, .T. ) ;
#77253=FILL_AREA_STYLE_COLOUR ( '', #80712 ) ;
#77409=DIRECTION ( 'NONE',  ( -0.7071067811865456854, 0.000000000000000000, 0.7071067811865493491 ) ) ;
#77849=EDGE_CURVE ( 'NONE', #102936, #8913, #51608, .T. ) ;
#78003=ORIENTED_EDGE ( 'NONE', *, *, #49733, .T. ) ;
#78112=MECHANICAL_DESIGN_GEOMETRIC_PRESENTATION_REPRESENTATION('',(#69502),#23014);
#78326=PRODUCT_DEFINITION_FORMATION_WITH_SPECIFIED_SOURCE ( 'ANY', '', #14054, .NOT_KNOWN. ) ;
#78450=CARTESIAN_POINT ( 'NONE',  ( 30.00000000000000000, 0.000000000000000000, 0.000000000000000000 ) ) ;
#78478=CARTESIAN_POINT ( 'NONE',  ( 28.99999999999999645, 0.000000000000000000, 4.999999999999999112 ) ) ;
#78692=VECTOR ( 'NONE', #94615, 1000.000000000000114 ) ;
#79157=( GEOMETRIC_REPRESENTATION_CONTEXT ( 3 ) GLOBAL_UNCERTAINTY_ASSIGNED_CONTEXT ( ( #101191 ) ) GLOBAL_UNIT_ASSIGNED_CONTEXT ( ( #94021, #79941, #12549 ) ) REPRESENTATION_CONTEXT ( 'NONE', 'WORKASPACE' ) );
#79272=FILL_AREA_STYLE ('',( #35671 ) ) ;
#79366=VECTOR ( 'NONE', #12829, 1000.000000000000114 ) ;
#79433=AXIS2_PLACEMENT_3D ( 'NONE', #28427, #3052, #45130 ) ;
#79941=( NAMED_UNIT ( * ) PLANE_ANGLE_UNIT ( ) SI_UNIT ( $, .RADIAN. ) );
#80264=CARTESIAN_POINT ( 'NONE',  ( 30.00000000000000000, 0.000000000000000000, 0.000000000000000000 ) ) ;
#80511=AXIS2_PLACEMENT_3D ( 'NONE', #44067, #11674, #13667 ) ;
#80625=ORIENTED_EDGE ( 'NONE', *, *, #101768, .F. ) ;
#80712=COLOUR_RGB ( '', 0.08235294, 0.09019608, 0.10196078) ;
#80829=( GEOMETRIC_REPRESENTATION_CONTEXT ( 3 ) GLOBAL_UNCERTAINTY_ASSIGNED_CONTEXT ( ( #12692 ) ) GLOBAL_UNIT_ASSIGNED_CONTEXT ( ( #65789, #24298, #57147 ) ) REPRESENTATION_CONTEXT ( 'NONE', 'WORKASPACE' ) );
#80952=CARTESIAN_POINT ( 'NONE',  ( -28.99999999999998934, 1.102182119232617714E-15, -9.000000000000000000 ) ) ;
#81095=( NAMED_UNIT ( * ) SI_UNIT ( $, .STERADIAN. ) SOLID_ANGLE_UNIT ( ) );
#81203=SHAPE_REPRESENTATION ( '14. Sleeve', ( #10728 ), #66095 ) ;
#81229=FILL_AREA_STYLE ('',( #89875 ) ) ;
#81600=PRESENTATION_STYLE_ASSIGNMENT (( #16357 ) ) ;
#81606=SURFACE_SIDE_STYLE ('',( #32585 ) ) ;
#81716=FILL_AREA_STYLE ('',( #8379 ) ) ;
#81769=DIRECTION ( 'NONE',  ( 0.000000000000000000, 0.000000000000000000, -1.000000000000000000 ) ) ;
#82155=FILL_AREA_STYLE ('',( #106425 ) ) ;
#82184=ORIENTED_EDGE ( 'NONE', *, *, #51509, .F. ) ;
#82203=MECHANICAL_DESIGN_GEOMETRIC_PRESENTATION_REPRESENTATION('',(#77062),#23654);
#82226=EDGE_LOOP ( 'NONE', ( #72854, #62259, #42995, #31719 ) ) ;
#82267=CARTESIAN_POINT ( 'NONE',  ( -30.00000000000000000, 0.000000000000000000, 0.000000000000000000 ) ) ;
#82506=( GEOMETRIC_REPRESENTATION_CONTEXT ( 3 ) GLOBAL_UNCERTAINTY_ASSIGNED_CONTEXT ( ( #42934 ) ) GLOBAL_UNIT_ASSIGNED_CONTEXT ( ( #59490, #75647, #76173 ) ) REPRESENTATION_CONTEXT ( 'NONE', 'WORKASPACE' ) );
#82668=CIRCLE ( 'NONE', #6904, 8.000000000000007105 ) ;
#82751=CARTESIAN_POINT ( 'NONE',  ( -30.00000000000000000, 0.000000000000000000, 0.000000000000000000 ) ) ;
#82762=AXIS2_PLACEMENT_3D ( 'NONE', #12554, #95102, #91509 ) ;
#82908=SURFACE_SIDE_STYLE ('',( #50003 ) ) ;
#83027=MECHANICAL_DESIGN_GEOMETRIC_PRESENTATION_REPRESENTATION('',(#39916),#69276);
#83193=( LENGTH_UNIT ( ) NAMED_UNIT ( * ) SI_UNIT ( .MILLI., .METRE. ) );
#83268=AXIS2_PLACEMENT_3D ( 'NONE', #82267, #49360, #105490 ) ;
#83401=VERTEX_POINT ( 'NONE', #84000 ) ;
#84000=CARTESIAN_POINT ( 'NONE',  ( 30.00000000000000000, 0.000000000000000000, -6.000000000000012434 ) ) ;
#84243=CARTESIAN_POINT ( 'NONE',  ( 30.00000000000000000, 0.000000000000000000, 9.000000000000000000 ) ) ;
#84529=( NAMED_UNIT ( * ) SI_UNIT ( $, .STERADIAN. ) SOLID_ANGLE_UNIT ( ) );
#84548=DIRECTION ( 'NONE',  ( 0.000000000000000000, 0.000000000000000000, -1.000000000000000000 ) ) ;
#84551=SURFACE_STYLE_FILL_AREA ( #3633 ) ;
#84552=EDGE_CURVE ( 'NONE', #28621, #85839, #91939, .T. ) ;
#84708=CARTESIAN_POINT ( 'NONE',  ( 29.00000000000001066, 1.102182119232617714E-15, -9.000000000000000000 ) ) ;
#84740=FILL_AREA_STYLE_COLOUR ( '', #21517 ) ;
#84765=DIRECTION ( 'NONE',  ( -1.000000000000000000, -0.000000000000000000, -0.000000000000000000 ) ) ;
#84806=DIRECTION ( 'NONE',  ( 0.000000000000000000, 0.000000000000000000, -1.000000000000000000 ) ) ;
#84812=DIRECTION ( 'NONE',  ( -1.000000000000000000, 0.000000000000000000, 0.000000000000000000 ) ) ;
#85054=DIRECTION ( 'NONE',  ( 0.000000000000000000, 0.000000000000000000, -1.000000000000000000 ) ) ;
#85351=( NAMED_UNIT ( * ) SI_UNIT ( $, .STERADIAN. ) SOLID_ANGLE_UNIT ( ) );
#85570=MECHANICAL_DESIGN_GEOMETRIC_PRESENTATION_REPRESENTATION('',(#73435),#99300);
#85573=EDGE_LOOP ( 'NONE', ( #67904, #7458, #72061, #78003 ) ) ;
#85602=SURFACE_SIDE_STYLE ('',( #5582 ) ) ;
#85708=COLOUR_RGB ( '', 0.66274510, 0.83137255, 0.94901961) ;
#85839=VERTEX_POINT ( 'NONE', #400 ) ;
#85892=MECHANICAL_DESIGN_GEOMETRIC_PRESENTATION_REPRESENTATION('',(#34241),#34311);
#85953=FILL_AREA_STYLE_COLOUR ( '', #67083 ) ;
#86490=PRESENTATION_STYLE_ASSIGNMENT (( #69749 ) ) ;
#86799=DIRECTION ( 'NONE',  ( 0.000000000000000000, 0.000000000000000000, -1.000000000000000000 ) ) ;
#87251=FILL_AREA_STYLE ('',( #53281 ) ) ;
#87697=VECTOR ( 'NONE', #95804, 1000.000000000000000 ) ;
#87903=ORIENTED_EDGE ( 'NONE', *, *, #50182, .F. ) ;
#87959=ORIENTED_EDGE ( 'NONE', *, *, #63182, .F. ) ;
#88057=DIRECTION ( 'NONE',  ( 0.000000000000000000, 0.000000000000000000, -1.000000000000000000 ) ) ;
#88153=VERTEX_POINT ( 'NONE', #98090 ) ;
#88243=EDGE_LOOP ( 'NONE', ( #10078, #93316, #9836, #29280 ) ) ;
#88623=STYLED_ITEM ( 'NONE', ( #76636 ), #27981 ) ;
#89182=CARTESIAN_POINT ( 'NONE',  ( 30.00000000000000000, 0.000000000000000000, 0.000000000000000000 ) ) ;
#89557=COLOUR_RGB ( '', 0.09019608, 0.27058824, 0.51372549) ;
#89725=AXIS2_PLACEMENT_3D ( 'NONE', #45645, #27377, #52121 ) ;
#89760=STYLED_ITEM ( 'NONE', ( #52125 ), #103525 ) ;
#89855=EDGE_CURVE ( 'NONE', #8913, #102936, #27376, .T. ) ;
#89875=FILL_AREA_STYLE_COLOUR ( '', #59901 ) ;
#90112=EDGE_CURVE ( 'NONE', #56343, #76051, #68886, .T. ) ;
#90367=( NAMED_UNIT ( * ) SI_UNIT ( $, .STERADIAN. ) SOLID_ANGLE_UNIT ( ) );
#90381=UNCERTAINTY_MEASURE_WITH_UNIT (LENGTH_MEASURE( 1.000000000000000082E-05 ), #69919, 'distance_accuracy_value', 'NONE');
#90800=DIRECTION ( 'NONE',  ( -1.000000000000000000, 0.000000000000000000, 0.000000000000000000 ) ) ;
#91054=( LENGTH_UNIT ( ) NAMED_UNIT ( * ) SI_UNIT ( .MILLI., .METRE. ) );
#91307=( NAMED_UNIT ( * ) PLANE_ANGLE_UNIT ( ) SI_UNIT ( $, .RADIAN. ) );
#91369=EDGE_CURVE ( 'NONE', #51789, #58408, #82668, .T. ) ;
#91509=DIRECTION ( 'NONE',  ( 0.000000000000000000, 0.000000000000000000, -1.000000000000000000 ) ) ;
#91648=AXIS2_PLACEMENT_3D ( 'NONE', #31494, #32010, #36549 ) ;
#91935=DIRECTION ( 'NONE',  ( -1.000000000000000000, -0.000000000000000000, -0.000000000000000000 ) ) ;
#91939=CIRCLE ( 'NONE', #76445, 4.999999999999999112 ) ;
#92283=UNCERTAINTY_MEASURE_WITH_UNIT (LENGTH_MEASURE( 1.000000000000000082E-05 ), #148, 'distance_accuracy_value', 'NONE');
#92361=EDGE_LOOP ( 'NONE', ( #36466, #70953, #39096, #80625 ) ) ;
#92457=VECTOR ( 'NONE', #99975, 1000.000000000000114 ) ;
#92589=FACE_BOUND ( 'NONE', #18041, .T. ) ;
#92600=DIRECTION ( 'NONE',  ( -1.000000000000000000, -0.000000000000000000, -0.000000000000000000 ) ) ;
#92609=VECTOR ( 'NONE', #53910, 1000.000000000000114 ) ;
#92938=STYLED_ITEM ( 'NONE', ( #86490 ), #32241 ) ;
#93167=SURFACE_STYLE_FILL_AREA ( #52163 ) ;
#93189=ORIENTED_EDGE ( 'NONE', *, *, #4137, .F. ) ;
#93316=ORIENTED_EDGE ( 'NONE', *, *, #49341, .T. ) ;
#93707=DIRECTION ( 'NONE',  ( -1.000000000000000000, -0.000000000000000000, -0.000000000000000000 ) ) ;
#93712=STYLED_ITEM ( 'NONE', ( #81600 ), #54999 ) ;
#94021=( LENGTH_UNIT ( ) NAMED_UNIT ( * ) SI_UNIT ( .MILLI., .METRE. ) );
#94140=AXIS2_PLACEMENT_3D ( 'NONE', #7412, #47869, #39811 ) ;
#94564=ORIENTED_EDGE ( 'NONE', *, *, #89855, .T. ) ;
#94615=DIRECTION ( 'NONE',  ( 0.7071067811865431318, 0.000000000000000000, -0.7071067811865517916 ) ) ;
#94660=MECHANICAL_DESIGN_GEOMETRIC_PRESENTATION_REPRESENTATION('',(#51589),#80829);
#94666=FACE_OUTER_BOUND ( 'NONE', #67534, .T. ) ;
#95102=DIRECTION ( 'NONE',  ( -1.000000000000000000, -0.000000000000000000, -0.000000000000000000 ) ) ;
#95221=DIRECTION ( 'NONE',  ( -1.000000000000000000, -0.000000000000000000, -0.000000000000000000 ) ) ;
#95284=CARTESIAN_POINT ( 'NONE',  ( -28.99999999999998934, 0.000000000000000000, -9.000000000000000000 ) ) ;
#95364=CARTESIAN_POINT ( 'NONE',  ( 28.99999999999999645, 6.123233995736765296E-16, 4.999999999999999112 ) ) ;
#95658=CARTESIAN_POINT ( 'NONE',  ( 28.99999999999999645, 0.000000000000000000, -4.999999999999999112 ) ) ;
#95727=PRODUCT_DEFINITION ( 'UNKNOWN', '', #78326, #74761 ) ;
#95804=DIRECTION ( 'NONE',  ( -1.000000000000000000, -0.000000000000000000, -0.000000000000000000 ) ) ;
#95858=FILL_AREA_STYLE_COLOUR ( '', #99524 ) ;
#96077=AXIS2_PLACEMENT_3D ( 'NONE', #72620, #105522, #31662 ) ;
#96557=UNCERTAINTY_MEASURE_WITH_UNIT (LENGTH_MEASURE( 1.000000000000000082E-05 ), #29563, 'distance_accuracy_value', 'NONE');
#96572=SURFACE_SIDE_STYLE ('',( #8603 ) ) ;
#96820=UNCERTAINTY_MEASURE_WITH_UNIT (LENGTH_MEASURE( 1.000000000000000082E-05 ), #8415, 'distance_accuracy_value', 'NONE');
#97050=ORIENTED_EDGE ( 'NONE', *, *, #77849, .T. ) ;
#97382=SURFACE_STYLE_USAGE ( .BOTH. , #55330 ) ;
#97450=CARTESIAN_POINT ( 'NONE',  ( 30.00000000000000000, 7.347880794884133541E-16, 6.000000000000012434 ) ) ;
#97602=PRESENTATION_STYLE_ASSIGNMENT (( #15102 ) ) ;
#97803=CYLINDRICAL_SURFACE ( 'NONE', #14373, 4.999999999999999112 ) ;
#98090=CARTESIAN_POINT ( 'NONE',  ( -30.00000000000000000, 0.000000000000000000, -7.999999999999986677 ) ) ;
#98166=( GEOMETRIC_REPRESENTATION_CONTEXT ( 3 ) GLOBAL_UNCERTAINTY_ASSIGNED_CONTEXT ( ( #76364 ) ) GLOBAL_UNIT_ASSIGNED_CONTEXT ( ( #44633, #68371, #10635 ) ) REPRESENTATION_CONTEXT ( 'NONE', 'WORKASPACE' ) );
#98497=( NAMED_UNIT ( * ) SI_UNIT ( $, .STERADIAN. ) SOLID_ANGLE_UNIT ( ) );
#98946=COLOUR_RGB ( '', 0.72549020, 0.75294118, 0.79215686) ;
#99021=SURFACE_STYLE_FILL_AREA ( #79272 ) ;
#99300=( GEOMETRIC_REPRESENTATION_CONTEXT ( 3 ) GLOBAL_UNCERTAINTY_ASSIGNED_CONTEXT ( ( #92283 ) ) GLOBAL_UNIT_ASSIGNED_CONTEXT ( ( #148, #15836, #81095 ) ) REPRESENTATION_CONTEXT ( 'NONE', 'WORKASPACE' ) );
#99343=AXIS2_PLACEMENT_3D ( 'NONE', #11534, #91935, #9949 ) ;
#99354=( NAMED_UNIT ( * ) SI_UNIT ( $, .STERADIAN. ) SOLID_ANGLE_UNIT ( ) );
#99380=FACE_OUTER_BOUND ( 'NONE', #55046, .T. ) ;
#99435=MECHANICAL_DESIGN_GEOMETRIC_PRESENTATION_REPRESENTATION('',(#102928),#63367);
#99524=COLOUR_RGB ( '', 0.31764706, 0.68627451, 0.89019608) ;
#99716=AXIS2_PLACEMENT_3D ( 'NONE', #71447, #95221, #6179 ) ;
#99775=EDGE_CURVE ( 'NONE', #85839, #28621, #6178, .T. ) ;
#99975=DIRECTION ( 'NONE',  ( -0.7071067811865456854, 0.000000000000000000, 0.7071067811865493491 ) ) ;
#100151=FACE_OUTER_BOUND ( 'NONE', #47415, .T. ) ;
#100440=FILL_AREA_STYLE ('',( #67559 ) ) ;
#100711=( NAMED_UNIT ( * ) SI_UNIT ( $, .STERADIAN. ) SOLID_ANGLE_UNIT ( ) );
#100995=( NAMED_UNIT ( * ) PLANE_ANGLE_UNIT ( ) SI_UNIT ( $, .RADIAN. ) );
#101007=AXIS2_PLACEMENT_3D ( 'NONE', #78450, #90800, #33115 ) ;
#101191=UNCERTAINTY_MEASURE_WITH_UNIT (LENGTH_MEASURE( 1.000000000000000082E-05 ), #94021, 'distance_accuracy_value', 'NONE');
#101204=UNCERTAINTY_MEASURE_WITH_UNIT (LENGTH_MEASURE( 1.000000000000000082E-05 ), #14337, 'distance_accuracy_value', 'NONE');
#101269=FACE_OUTER_BOUND ( 'NONE', #88243, .T. ) ;
#101344=ORIENTED_EDGE ( 'NONE', *, *, #49733, .F. ) ;
#101482=CARTESIAN_POINT ( 'NONE',  ( 30.00000000000000000, 0.000000000000000000, 4.999999999999999112 ) ) ;
#101529=FILL_AREA_STYLE ('',( #77253 ) ) ;
#101570=MECHANICAL_DESIGN_GEOMETRIC_PRESENTATION_REPRESENTATION('',(#92938),#79157);
#101598=CIRCLE ( 'NONE', #55065, 7.999999999999986677 ) ;
#101768=EDGE_CURVE ( 'NONE', #85839, #83401, #102685, .T. ) ;
#102214=EDGE_LOOP ( 'NONE', ( #93189, #12298, #65346, #39444 ) ) ;
#102279=( NAMED_UNIT ( * ) PLANE_ANGLE_UNIT ( ) SI_UNIT ( $, .RADIAN. ) );
#102404=AXIS2_PLACEMENT_3D ( 'NONE', #51827, #41623, #33549 ) ;
#102685=LINE ( 'NONE', #95658, #78692 ) ;
#102928=STYLED_ITEM ( 'NONE', ( #64546 ), #26328 ) ;
#102936=VERTEX_POINT ( 'NONE', #29103 ) ;
#103525=ADVANCED_FACE ( 'NONE', ( #92589, #100151 ), #50518, .T. ) ;
#103533=DIRECTION ( 'NONE',  ( 0.000000000000000000, 0.000000000000000000, -1.000000000000000000 ) ) ;
#103653=COLOUR_RGB ( '', 0.72549020, 0.75294118, 0.79215686) ;
#103926=ORIENTED_EDGE ( 'NONE', *, *, #4137, .T. ) ;
#104274=FILL_AREA_STYLE_COLOUR ( '', #85708 ) ;
#104646=CYLINDRICAL_SURFACE ( 'NONE', #17121, 4.999999999999999112 ) ;
#104694=( GEOMETRIC_REPRESENTATION_CONTEXT ( 3 ) GLOBAL_UNCERTAINTY_ASSIGNED_CONTEXT ( ( #96557 ) ) GLOBAL_UNIT_ASSIGNED_CONTEXT ( ( #29563, #39225, #62434 ) ) REPRESENTATION_CONTEXT ( 'NONE', 'WORKASPACE' ) );
#105170=CIRCLE ( 'NONE', #82762, 6.000000000000012434 ) ;
#105187=CARTESIAN_POINT ( 'NONE',  ( 30.00000000000000000, 0.000000000000000000, 0.000000000000000000 ) ) ;
#105490=DIRECTION ( 'NONE',  ( 0.000000000000000000, 0.000000000000000000, 1.000000000000000000 ) ) ;
#105522=DIRECTION ( 'NONE',  ( 1.000000000000000000, 0.000000000000000000, 0.000000000000000000 ) ) ;
#105806=AXIS2_PLACEMENT_3D ( 'NONE', #80264, #56518, #73770 ) ;
#106425=FILL_AREA_STYLE_COLOUR ( '', #40730 ) ;
#106587=CONICAL_SURFACE ( 'NONE', #34343, 8.000000000000007105, 0.7853981633974509435 ) ;
ENDSEC;
END-ISO-10303-21;
